ISO-10303-21;
HEADER;
/* Generated by software containing ST-Developer
 * from STEP Tools, Inc. (www.steptools.com) 
 */

FILE_DESCRIPTION(
/* description */ ('Worm-less right-angle friction wheel drive'),
/* implementation_level */ '2;1');

FILE_NAME(
/* name */ 'Input bearing carrier (1).step',
/* time_stamp */ '2026-10-28T03:22:36-07:00',
/* author */ (''),
/* organization */ (''),
/* preprocessor_version */ 'ST-DEVELOPER v20.2',
/* originating_system */ 'Autodesk Translation Framework v15.17.0.0',
/* authorisation */ '');

FILE_SCHEMA (('AUTOMOTIVE_DESIGN { 1 0 10303 214 3 1 1 }'));
ENDSEC;

DATA;
#10=MECHANICAL_DESIGN_GEOMETRIC_PRESENTATION_REPRESENTATION('',(#618),#17046);
#524=SHAPE_REPRESENTATION_RELATIONSHIP('SRR','None',#17267,#571);
#571=ADVANCED_BREP_SHAPE_REPRESENTATION('',(#672),#17003);
#618=STYLED_ITEM('',(#17591),#672);
#672=MANIFOLD_SOLID_BREP('Body1',#8173);
#787=FACE_BOUND('',#1845,.T.);
#788=FACE_BOUND('',#1847,.T.);
#789=FACE_BOUND('',#1851,.T.);
#790=FACE_BOUND('',#1852,.T.);
#791=FACE_BOUND('',#1853,.T.);
#792=FACE_BOUND('',#1854,.T.);
#793=FACE_BOUND('',#1855,.T.);
#794=FACE_BOUND('',#1858,.T.);
#795=FACE_BOUND('',#1859,.T.);
#796=FACE_BOUND('',#1860,.T.);
#797=FACE_BOUND('',#1861,.T.);
#798=FACE_BOUND('',#1862,.T.);
#799=FACE_BOUND('',#1866,.T.);
#800=FACE_BOUND('',#1867,.T.);
#1000=PLANE('',#8950);
#1001=PLANE('',#8951);
#1002=PLANE('',#8952);
#1003=PLANE('',#8953);
#1004=PLANE('',#8954);
#1005=PLANE('',#8955);
#1006=PLANE('',#8956);
#1007=PLANE('',#8957);
#1008=PLANE('',#8958);
#1009=PLANE('',#8959);
#1299=FACE_OUTER_BOUND('',#1837,.T.);
#1300=FACE_OUTER_BOUND('',#1838,.T.);
#1301=FACE_OUTER_BOUND('',#1839,.T.);
#1302=FACE_OUTER_BOUND('',#1840,.T.);
#1303=FACE_OUTER_BOUND('',#1841,.T.);
#1304=FACE_OUTER_BOUND('',#1842,.T.);
#1305=FACE_OUTER_BOUND('',#1843,.T.);
#1306=FACE_OUTER_BOUND('',#1844,.T.);
#1307=FACE_OUTER_BOUND('',#1846,.T.);
#1308=FACE_OUTER_BOUND('',#1848,.T.);
#1309=FACE_OUTER_BOUND('',#1849,.T.);
#1310=FACE_OUTER_BOUND('',#1850,.T.);
#1311=FACE_OUTER_BOUND('',#1856,.T.);
#1312=FACE_OUTER_BOUND('',#1857,.T.);
#1313=FACE_OUTER_BOUND('',#1863,.T.);
#1314=FACE_OUTER_BOUND('',#1864,.T.);
#1315=FACE_OUTER_BOUND('',#1865,.T.);
#1837=EDGE_LOOP('',(#5984,#5985,#5986,#5987));
#1838=EDGE_LOOP('',(#5988,#5989,#5990,#5991));
#1839=EDGE_LOOP('',(#5992,#5993,#5994,#5995));
#1840=EDGE_LOOP('',(#5996,#5997,#5998,#5999));
#1841=EDGE_LOOP('',(#6000,#6001,#6002,#6003));
#1842=EDGE_LOOP('',(#6004,#6005,#6006,#6007));
#1843=EDGE_LOOP('',(#6008,#6009,#6010,#6011));
#1844=EDGE_LOOP('',(#6012,#6013,#6014,#6015));
#1845=EDGE_LOOP('',(#6016));
#1846=EDGE_LOOP('',(#6017,#6018,#6019,#6020));
#1847=EDGE_LOOP('',(#6021));
#1848=EDGE_LOOP('',(#6022,#6023,#6024,#6025));
#1849=EDGE_LOOP('',(#6026,#6027,#6028,#6029));
#1850=EDGE_LOOP('',(#6030,#6031,#6032,#6033,#6034,#6035,#6036,#6037));
#1851=EDGE_LOOP('',(#6038));
#1852=EDGE_LOOP('',(#6039));
#1853=EDGE_LOOP('',(#6040));
#1854=EDGE_LOOP('',(#6041));
#1855=EDGE_LOOP('',(#6042));
#1856=EDGE_LOOP('',(#6043,#6044,#6045,#6046));
#1857=EDGE_LOOP('',(#6047,#6048,#6049,#6050,#6051,#6052,#6053,#6054));
#1858=EDGE_LOOP('',(#6055));
#1859=EDGE_LOOP('',(#6056));
#1860=EDGE_LOOP('',(#6057));
#1861=EDGE_LOOP('',(#6058));
#1862=EDGE_LOOP('',(#6059));
#1863=EDGE_LOOP('',(#6060,#6061,#6062,#6063));
#1864=EDGE_LOOP('',(#6064,#6065,#6066,#6067));
#1865=EDGE_LOOP('',(#6068,#6069,#6070,#6071));
#1866=EDGE_LOOP('',(#6072));
#1867=EDGE_LOOP('',(#6073));
#2516=LINE('',#12855,#3056);
#2517=LINE('',#12861,#3057);
#2518=LINE('',#12867,#3058);
#2519=LINE('',#12873,#3059);
#2520=LINE('',#12879,#3060);
#2521=LINE('',#12885,#3061);
#2522=LINE('',#12891,#3062);
#2523=LINE('',#12896,#3063);
#2524=LINE('',#12898,#3064);
#2525=LINE('',#12900,#3065);
#2526=LINE('',#12901,#3066);
#2527=LINE('',#12905,#3067);
#2528=LINE('',#12907,#3068);
#2529=LINE('',#12909,#3069);
#2530=LINE('',#12910,#3070);
#2531=LINE('',#12913,#3071);
#2532=LINE('',#12915,#3072);
#2533=LINE('',#12916,#3073);
#2534=LINE('',#12919,#3074);
#2535=LINE('',#12921,#3075);
#2536=LINE('',#12922,#3076);
#2537=LINE('',#12925,#3077);
#2538=LINE('',#12927,#3078);
#2539=LINE('',#12928,#3079);
#2540=LINE('',#12929,#3080);
#2541=LINE('',#12932,#3081);
#2542=LINE('',#12933,#3082);
#2543=LINE('',#12936,#3083);
#2544=LINE('',#12937,#3084);
#2545=LINE('',#12938,#3085);
#2546=LINE('',#12940,#3086);
#3056=VECTOR('',#10290,0.165);
#3057=VECTOR('',#10297,0.165);
#3058=VECTOR('',#10304,0.165);
#3059=VECTOR('',#10311,0.165);
#3060=VECTOR('',#10318,1.6);
#3061=VECTOR('',#10325,0.225);
#3062=VECTOR('',#10332,0.225);
#3063=VECTOR('',#10337,1.);
#3064=VECTOR('',#10338,1.);
#3065=VECTOR('',#10339,1.);
#3066=VECTOR('',#10340,1.);
#3067=VECTOR('',#10343,1.);
#3068=VECTOR('',#10344,1.);
#3069=VECTOR('',#10345,1.);
#3070=VECTOR('',#10346,1.);
#3071=VECTOR('',#10349,1.);
#3072=VECTOR('',#10350,1.);
#3073=VECTOR('',#10351,1.);
#3074=VECTOR('',#10354,1.);
#3075=VECTOR('',#10355,1.);
#3076=VECTOR('',#10356,1.);
#3077=VECTOR('',#10359,1.);
#3078=VECTOR('',#10360,1.);
#3079=VECTOR('',#10361,1.);
#3080=VECTOR('',#10362,1.);
#3081=VECTOR('',#10365,1.);
#3082=VECTOR('',#10366,1.);
#3083=VECTOR('',#10369,1.);
#3084=VECTOR('',#10370,1.);
#3085=VECTOR('',#10371,1.);
#3086=VECTOR('',#10374,1.);
#3543=CIRCLE('',#8930,0.165);
#3544=CIRCLE('',#8931,0.165);
#3545=CIRCLE('',#8933,0.165);
#3546=CIRCLE('',#8934,0.165);
#3547=CIRCLE('',#8936,0.165);
#3548=CIRCLE('',#8937,0.165);
#3549=CIRCLE('',#8939,0.165);
#3550=CIRCLE('',#8940,0.165);
#3551=CIRCLE('',#8942,1.6);
#3552=CIRCLE('',#8943,1.6);
#3553=CIRCLE('',#8945,0.225);
#3554=CIRCLE('',#8946,0.225);
#3555=CIRCLE('',#8948,0.225);
#3556=CIRCLE('',#8949,0.225);
#4019=VERTEX_POINT('',#12852);
#4020=VERTEX_POINT('',#12854);
#4021=VERTEX_POINT('',#12858);
#4022=VERTEX_POINT('',#12860);
#4023=VERTEX_POINT('',#12864);
#4024=VERTEX_POINT('',#12866);
#4025=VERTEX_POINT('',#12870);
#4026=VERTEX_POINT('',#12872);
#4027=VERTEX_POINT('',#12876);
#4028=VERTEX_POINT('',#12878);
#4029=VERTEX_POINT('',#12882);
#4030=VERTEX_POINT('',#12884);
#4031=VERTEX_POINT('',#12888);
#4032=VERTEX_POINT('',#12890);
#4033=VERTEX_POINT('',#12894);
#4034=VERTEX_POINT('',#12895);
#4035=VERTEX_POINT('',#12897);
#4036=VERTEX_POINT('',#12899);
#4037=VERTEX_POINT('',#12903);
#4038=VERTEX_POINT('',#12904);
#4039=VERTEX_POINT('',#12906);
#4040=VERTEX_POINT('',#12908);
#4041=VERTEX_POINT('',#12912);
#4042=VERTEX_POINT('',#12914);
#4043=VERTEX_POINT('',#12918);
#4044=VERTEX_POINT('',#12920);
#4045=VERTEX_POINT('',#12924);
#4046=VERTEX_POINT('',#12926);
#4047=VERTEX_POINT('',#12931);
#4048=VERTEX_POINT('',#12935);
#4761=EDGE_CURVE('',#4019,#4019,#3543,.T.);
#4762=EDGE_CURVE('',#4019,#4020,#2516,.T.);
#4763=EDGE_CURVE('',#4020,#4020,#3544,.T.);
#4764=EDGE_CURVE('',#4021,#4021,#3545,.T.);
#4765=EDGE_CURVE('',#4021,#4022,#2517,.T.);
#4766=EDGE_CURVE('',#4022,#4022,#3546,.T.);
#4767=EDGE_CURVE('',#4023,#4023,#3547,.T.);
#4768=EDGE_CURVE('',#4023,#4024,#2518,.T.);
#4769=EDGE_CURVE('',#4024,#4024,#3548,.T.);
#4770=EDGE_CURVE('',#4025,#4025,#3549,.T.);
#4771=EDGE_CURVE('',#4025,#4026,#2519,.T.);
#4772=EDGE_CURVE('',#4026,#4026,#3550,.T.);
#4773=EDGE_CURVE('',#4027,#4027,#3551,.T.);
#4774=EDGE_CURVE('',#4027,#4028,#2520,.T.);
#4775=EDGE_CURVE('',#4028,#4028,#3552,.T.);
#4776=EDGE_CURVE('',#4029,#4029,#3553,.T.);
#4777=EDGE_CURVE('',#4029,#4030,#2521,.T.);
#4778=EDGE_CURVE('',#4030,#4030,#3554,.T.);
#4779=EDGE_CURVE('',#4031,#4031,#3555,.T.);
#4780=EDGE_CURVE('',#4031,#4032,#2522,.T.);
#4781=EDGE_CURVE('',#4032,#4032,#3556,.T.);
#4782=EDGE_CURVE('',#4033,#4034,#2523,.T.);
#4783=EDGE_CURVE('',#4035,#4033,#2524,.T.);
#4784=EDGE_CURVE('',#4035,#4036,#2525,.T.);
#4785=EDGE_CURVE('',#4034,#4036,#2526,.T.);
#4786=EDGE_CURVE('',#4037,#4038,#2527,.T.);
#4787=EDGE_CURVE('',#4039,#4037,#2528,.T.);
#4788=EDGE_CURVE('',#4040,#4039,#2529,.T.);
#4789=EDGE_CURVE('',#4038,#4040,#2530,.T.);
#4790=EDGE_CURVE('',#4040,#4041,#2531,.T.);
#4791=EDGE_CURVE('',#4042,#4039,#2532,.T.);
#4792=EDGE_CURVE('',#4041,#4042,#2533,.T.);
#4793=EDGE_CURVE('',#4043,#4035,#2534,.T.);
#4794=EDGE_CURVE('',#4043,#4044,#2535,.T.);
#4795=EDGE_CURVE('',#4036,#4044,#2536,.T.);
#4796=EDGE_CURVE('',#4033,#4045,#2537,.T.);
#4797=EDGE_CURVE('',#4046,#4045,#2538,.T.);
#4798=EDGE_CURVE('',#4038,#4046,#2539,.T.);
#4799=EDGE_CURVE('',#4041,#4043,#2540,.T.);
#4800=EDGE_CURVE('',#4034,#4047,#2541,.T.);
#4801=EDGE_CURVE('',#4045,#4047,#2542,.T.);
#4802=EDGE_CURVE('',#4037,#4048,#2543,.T.);
#4803=EDGE_CURVE('',#4047,#4048,#2544,.T.);
#4804=EDGE_CURVE('',#4044,#4042,#2545,.T.);
#4805=EDGE_CURVE('',#4048,#4046,#2546,.T.);
#5984=ORIENTED_EDGE('',*,*,#4761,.F.);
#5985=ORIENTED_EDGE('',*,*,#4762,.T.);
#5986=ORIENTED_EDGE('',*,*,#4763,.F.);
#5987=ORIENTED_EDGE('',*,*,#4762,.F.);
#5988=ORIENTED_EDGE('',*,*,#4764,.F.);
#5989=ORIENTED_EDGE('',*,*,#4765,.T.);
#5990=ORIENTED_EDGE('',*,*,#4766,.F.);
#5991=ORIENTED_EDGE('',*,*,#4765,.F.);
#5992=ORIENTED_EDGE('',*,*,#4767,.F.);
#5993=ORIENTED_EDGE('',*,*,#4768,.T.);
#5994=ORIENTED_EDGE('',*,*,#4769,.F.);
#5995=ORIENTED_EDGE('',*,*,#4768,.F.);
#5996=ORIENTED_EDGE('',*,*,#4770,.F.);
#5997=ORIENTED_EDGE('',*,*,#4771,.T.);
#5998=ORIENTED_EDGE('',*,*,#4772,.F.);
#5999=ORIENTED_EDGE('',*,*,#4771,.F.);
#6000=ORIENTED_EDGE('',*,*,#4773,.F.);
#6001=ORIENTED_EDGE('',*,*,#4774,.T.);
#6002=ORIENTED_EDGE('',*,*,#4775,.F.);
#6003=ORIENTED_EDGE('',*,*,#4774,.F.);
#6004=ORIENTED_EDGE('',*,*,#4776,.F.);
#6005=ORIENTED_EDGE('',*,*,#4777,.T.);
#6006=ORIENTED_EDGE('',*,*,#4778,.F.);
#6007=ORIENTED_EDGE('',*,*,#4777,.F.);
#6008=ORIENTED_EDGE('',*,*,#4779,.F.);
#6009=ORIENTED_EDGE('',*,*,#4780,.T.);
#6010=ORIENTED_EDGE('',*,*,#4781,.F.);
#6011=ORIENTED_EDGE('',*,*,#4780,.F.);
#6012=ORIENTED_EDGE('',*,*,#4782,.F.);
#6013=ORIENTED_EDGE('',*,*,#4783,.F.);
#6014=ORIENTED_EDGE('',*,*,#4784,.T.);
#6015=ORIENTED_EDGE('',*,*,#4785,.F.);
#6016=ORIENTED_EDGE('',*,*,#4781,.T.);
#6017=ORIENTED_EDGE('',*,*,#4786,.F.);
#6018=ORIENTED_EDGE('',*,*,#4787,.F.);
#6019=ORIENTED_EDGE('',*,*,#4788,.F.);
#6020=ORIENTED_EDGE('',*,*,#4789,.F.);
#6021=ORIENTED_EDGE('',*,*,#4778,.T.);
#6022=ORIENTED_EDGE('',*,*,#4790,.F.);
#6023=ORIENTED_EDGE('',*,*,#4788,.T.);
#6024=ORIENTED_EDGE('',*,*,#4791,.F.);
#6025=ORIENTED_EDGE('',*,*,#4792,.F.);
#6026=ORIENTED_EDGE('',*,*,#4793,.F.);
#6027=ORIENTED_EDGE('',*,*,#4794,.T.);
#6028=ORIENTED_EDGE('',*,*,#4795,.F.);
#6029=ORIENTED_EDGE('',*,*,#4784,.F.);
#6030=ORIENTED_EDGE('',*,*,#4796,.T.);
#6031=ORIENTED_EDGE('',*,*,#4797,.F.);
#6032=ORIENTED_EDGE('',*,*,#4798,.F.);
#6033=ORIENTED_EDGE('',*,*,#4789,.T.);
#6034=ORIENTED_EDGE('',*,*,#4790,.T.);
#6035=ORIENTED_EDGE('',*,*,#4799,.T.);
#6036=ORIENTED_EDGE('',*,*,#4793,.T.);
#6037=ORIENTED_EDGE('',*,*,#4783,.T.);
#6038=ORIENTED_EDGE('',*,*,#4773,.T.);
#6039=ORIENTED_EDGE('',*,*,#4770,.T.);
#6040=ORIENTED_EDGE('',*,*,#4767,.T.);
#6041=ORIENTED_EDGE('',*,*,#4764,.T.);
#6042=ORIENTED_EDGE('',*,*,#4761,.T.);
#6043=ORIENTED_EDGE('',*,*,#4782,.T.);
#6044=ORIENTED_EDGE('',*,*,#4800,.T.);
#6045=ORIENTED_EDGE('',*,*,#4801,.F.);
#6046=ORIENTED_EDGE('',*,*,#4796,.F.);
#6047=ORIENTED_EDGE('',*,*,#4802,.T.);
#6048=ORIENTED_EDGE('',*,*,#4803,.F.);
#6049=ORIENTED_EDGE('',*,*,#4800,.F.);
#6050=ORIENTED_EDGE('',*,*,#4785,.T.);
#6051=ORIENTED_EDGE('',*,*,#4795,.T.);
#6052=ORIENTED_EDGE('',*,*,#4804,.T.);
#6053=ORIENTED_EDGE('',*,*,#4791,.T.);
#6054=ORIENTED_EDGE('',*,*,#4787,.T.);
#6055=ORIENTED_EDGE('',*,*,#4775,.T.);
#6056=ORIENTED_EDGE('',*,*,#4772,.T.);
#6057=ORIENTED_EDGE('',*,*,#4769,.T.);
#6058=ORIENTED_EDGE('',*,*,#4766,.T.);
#6059=ORIENTED_EDGE('',*,*,#4763,.T.);
#6060=ORIENTED_EDGE('',*,*,#4786,.T.);
#6061=ORIENTED_EDGE('',*,*,#4798,.T.);
#6062=ORIENTED_EDGE('',*,*,#4805,.F.);
#6063=ORIENTED_EDGE('',*,*,#4802,.F.);
#6064=ORIENTED_EDGE('',*,*,#4805,.T.);
#6065=ORIENTED_EDGE('',*,*,#4797,.T.);
#6066=ORIENTED_EDGE('',*,*,#4801,.T.);
#6067=ORIENTED_EDGE('',*,*,#4803,.T.);
#6068=ORIENTED_EDGE('',*,*,#4804,.F.);
#6069=ORIENTED_EDGE('',*,*,#4794,.F.);
#6070=ORIENTED_EDGE('',*,*,#4799,.F.);
#6071=ORIENTED_EDGE('',*,*,#4792,.T.);
#6072=ORIENTED_EDGE('',*,*,#4776,.T.);
#6073=ORIENTED_EDGE('',*,*,#4779,.T.);
#7573=CYLINDRICAL_SURFACE('',#8929,0.165);
#7574=CYLINDRICAL_SURFACE('',#8932,0.165);
#7575=CYLINDRICAL_SURFACE('',#8935,0.165);
#7576=CYLINDRICAL_SURFACE('',#8938,0.165);
#7577=CYLINDRICAL_SURFACE('',#8941,1.6);
#7578=CYLINDRICAL_SURFACE('',#8944,0.225);
#7579=CYLINDRICAL_SURFACE('',#8947,0.225);
#7791=ADVANCED_FACE('',(#1299),#7573,.F.);
#7792=ADVANCED_FACE('',(#1300),#7574,.F.);
#7793=ADVANCED_FACE('',(#1301),#7575,.F.);
#7794=ADVANCED_FACE('',(#1302),#7576,.F.);
#7795=ADVANCED_FACE('',(#1303),#7577,.F.);
#7796=ADVANCED_FACE('',(#1304),#7578,.F.);
#7797=ADVANCED_FACE('',(#1305),#7579,.F.);
#7798=ADVANCED_FACE('',(#1306,#787),#1000,.T.);
#7799=ADVANCED_FACE('',(#1307,#788),#1001,.T.);
#7800=ADVANCED_FACE('',(#1308),#1002,.T.);
#7801=ADVANCED_FACE('',(#1309),#1003,.T.);
#7802=ADVANCED_FACE('',(#1310,#789,#790,#791,#792,#793),#1004,.T.);
#7803=ADVANCED_FACE('',(#1311),#1005,.T.);
#7804=ADVANCED_FACE('',(#1312,#794,#795,#796,#797,#798),#1006,.T.);
#7805=ADVANCED_FACE('',(#1313),#1007,.T.);
#7806=ADVANCED_FACE('',(#1314),#1008,.T.);
#7807=ADVANCED_FACE('',(#1315,#799,#800),#1009,.F.);
#8173=CLOSED_SHELL('',(#7791,#7792,#7793,#7794,#7795,#7796,#7797,#7798,
#7799,#7800,#7801,#7802,#7803,#7804,#7805,#7806,#7807));
#8928=AXIS2_PLACEMENT_3D('',#12850,#10284,#10285);
#8929=AXIS2_PLACEMENT_3D('',#12851,#10286,#10287);
#8930=AXIS2_PLACEMENT_3D('',#12853,#10288,#10289);
#8931=AXIS2_PLACEMENT_3D('',#12856,#10291,#10292);
#8932=AXIS2_PLACEMENT_3D('',#12857,#10293,#10294);
#8933=AXIS2_PLACEMENT_3D('',#12859,#10295,#10296);
#8934=AXIS2_PLACEMENT_3D('',#12862,#10298,#10299);
#8935=AXIS2_PLACEMENT_3D('',#12863,#10300,#10301);
#8936=AXIS2_PLACEMENT_3D('',#12865,#10302,#10303);
#8937=AXIS2_PLACEMENT_3D('',#12868,#10305,#10306);
#8938=AXIS2_PLACEMENT_3D('',#12869,#10307,#10308);
#8939=AXIS2_PLACEMENT_3D('',#12871,#10309,#10310);
#8940=AXIS2_PLACEMENT_3D('',#12874,#10312,#10313);
#8941=AXIS2_PLACEMENT_3D('',#12875,#10314,#10315);
#8942=AXIS2_PLACEMENT_3D('',#12877,#10316,#10317);
#8943=AXIS2_PLACEMENT_3D('',#12880,#10319,#10320);
#8944=AXIS2_PLACEMENT_3D('',#12881,#10321,#10322);
#8945=AXIS2_PLACEMENT_3D('',#12883,#10323,#10324);
#8946=AXIS2_PLACEMENT_3D('',#12886,#10326,#10327);
#8947=AXIS2_PLACEMENT_3D('',#12887,#10328,#10329);
#8948=AXIS2_PLACEMENT_3D('',#12889,#10330,#10331);
#8949=AXIS2_PLACEMENT_3D('',#12892,#10333,#10334);
#8950=AXIS2_PLACEMENT_3D('',#12893,#10335,#10336);
#8951=AXIS2_PLACEMENT_3D('',#12902,#10341,#10342);
#8952=AXIS2_PLACEMENT_3D('',#12911,#10347,#10348);
#8953=AXIS2_PLACEMENT_3D('',#12917,#10352,#10353);
#8954=AXIS2_PLACEMENT_3D('',#12923,#10357,#10358);
#8955=AXIS2_PLACEMENT_3D('',#12930,#10363,#10364);
#8956=AXIS2_PLACEMENT_3D('',#12934,#10367,#10368);
#8957=AXIS2_PLACEMENT_3D('',#12939,#10372,#10373);
#8958=AXIS2_PLACEMENT_3D('',#12941,#10375,#10376);
#8959=AXIS2_PLACEMENT_3D('',#12942,#10377,#10378);
#10284=DIRECTION('axis',(0.,0.,1.));
#10285=DIRECTION('refdir',(1.,0.,0.));
#10286=DIRECTION('center_axis',(0.,1.,0.));
#10287=DIRECTION('ref_axis',(1.,0.,0.));
#10288=DIRECTION('center_axis',(0.,1.,0.));
#10289=DIRECTION('ref_axis',(1.,0.,0.));
#10290=DIRECTION('',(0.,1.,0.));
#10291=DIRECTION('center_axis',(0.,-1.,0.));
#10292=DIRECTION('ref_axis',(1.,0.,0.));
#10293=DIRECTION('center_axis',(0.,1.,0.));
#10294=DIRECTION('ref_axis',(1.,0.,0.));
#10295=DIRECTION('center_axis',(0.,1.,0.));
#10296=DIRECTION('ref_axis',(1.,0.,0.));
#10297=DIRECTION('',(0.,1.,0.));
#10298=DIRECTION('center_axis',(0.,-1.,0.));
#10299=DIRECTION('ref_axis',(1.,0.,0.));
#10300=DIRECTION('center_axis',(0.,1.,0.));
#10301=DIRECTION('ref_axis',(1.,0.,0.));
#10302=DIRECTION('center_axis',(0.,1.,0.));
#10303=DIRECTION('ref_axis',(1.,0.,0.));
#10304=DIRECTION('',(0.,1.,0.));
#10305=DIRECTION('center_axis',(0.,-1.,0.));
#10306=DIRECTION('ref_axis',(1.,0.,0.));
#10307=DIRECTION('center_axis',(0.,1.,0.));
#10308=DIRECTION('ref_axis',(1.,0.,0.));
#10309=DIRECTION('center_axis',(0.,1.,0.));
#10310=DIRECTION('ref_axis',(1.,0.,0.));
#10311=DIRECTION('',(0.,1.,0.));
#10312=DIRECTION('center_axis',(0.,-1.,0.));
#10313=DIRECTION('ref_axis',(1.,0.,0.));
#10314=DIRECTION('center_axis',(0.,1.,0.));
#10315=DIRECTION('ref_axis',(1.,0.,0.));
#10316=DIRECTION('center_axis',(0.,1.,0.));
#10317=DIRECTION('ref_axis',(1.,0.,0.));
#10318=DIRECTION('',(0.,1.,0.));
#10319=DIRECTION('center_axis',(0.,-1.,0.));
#10320=DIRECTION('ref_axis',(1.,0.,0.));
#10321=DIRECTION('center_axis',(0.,0.,1.));
#10322=DIRECTION('ref_axis',(1.,0.,0.));
#10323=DIRECTION('center_axis',(0.,0.,1.));
#10324=DIRECTION('ref_axis',(1.,0.,0.));
#10325=DIRECTION('',(0.,0.,1.));
#10326=DIRECTION('center_axis',(0.,0.,-1.));
#10327=DIRECTION('ref_axis',(1.,0.,0.));
#10328=DIRECTION('center_axis',(0.,0.,1.));
#10329=DIRECTION('ref_axis',(1.,0.,0.));
#10330=DIRECTION('center_axis',(0.,0.,1.));
#10331=DIRECTION('ref_axis',(1.,0.,0.));
#10332=DIRECTION('',(0.,0.,1.));
#10333=DIRECTION('center_axis',(0.,0.,-1.));
#10334=DIRECTION('ref_axis',(1.,0.,0.));
#10335=DIRECTION('center_axis',(0.,0.,1.));
#10336=DIRECTION('ref_axis',(1.,0.,0.));
#10337=DIRECTION('',(0.,1.,0.));
#10338=DIRECTION('',(-1.,0.,0.));
#10339=DIRECTION('',(0.,1.,0.));
#10340=DIRECTION('',(1.,0.,0.));
#10341=DIRECTION('center_axis',(0.,0.,1.));
#10342=DIRECTION('ref_axis',(1.,0.,0.));
#10343=DIRECTION('',(0.,-1.,0.));
#10344=DIRECTION('',(1.,0.,0.));
#10345=DIRECTION('',(0.,1.,0.));
#10346=DIRECTION('',(-1.,0.,0.));
#10347=DIRECTION('center_axis',(-1.,0.,0.));
#10348=DIRECTION('ref_axis',(0.,0.,1.));
#10349=DIRECTION('',(0.,0.,-1.));
#10350=DIRECTION('',(0.,0.,1.));
#10351=DIRECTION('',(0.,1.,0.));
#10352=DIRECTION('center_axis',(1.,0.,0.));
#10353=DIRECTION('ref_axis',(0.,0.,-1.));
#10354=DIRECTION('',(0.,0.,1.));
#10355=DIRECTION('',(0.,1.,0.));
#10356=DIRECTION('',(0.,0.,-1.));
#10357=DIRECTION('center_axis',(0.,-1.,0.));
#10358=DIRECTION('ref_axis',(1.,0.,0.));
#10359=DIRECTION('',(0.,0.,1.));
#10360=DIRECTION('',(1.,0.,0.));
#10361=DIRECTION('',(0.,0.,1.));
#10362=DIRECTION('',(1.,0.,0.));
#10363=DIRECTION('center_axis',(1.,0.,0.));
#10364=DIRECTION('ref_axis',(0.,1.,0.));
#10365=DIRECTION('',(0.,0.,1.));
#10366=DIRECTION('',(0.,1.,0.));
#10367=DIRECTION('center_axis',(0.,1.,0.));
#10368=DIRECTION('ref_axis',(-1.,0.,0.));
#10369=DIRECTION('',(0.,0.,1.));
#10370=DIRECTION('',(-1.,0.,0.));
#10371=DIRECTION('',(-1.,0.,0.));
#10372=DIRECTION('center_axis',(-1.,0.,0.));
#10373=DIRECTION('ref_axis',(0.,-1.,0.));
#10374=DIRECTION('',(0.,-1.,0.));
#10375=DIRECTION('center_axis',(0.,0.,1.));
#10376=DIRECTION('ref_axis',(1.,0.,0.));
#10377=DIRECTION('center_axis',(0.,0.,1.));
#10378=DIRECTION('ref_axis',(1.,0.,0.));
#12850=CARTESIAN_POINT('',(0.,0.,0.));
#12851=CARTESIAN_POINT('Origin',(-1.48492424049175,-4.9,5.51507575950825));
#12852=CARTESIAN_POINT('',(-1.64992424049175,-4.8,5.51507575950825));
#12853=CARTESIAN_POINT('Origin',(-1.48492424049175,-4.8,5.51507575950825));
#12854=CARTESIAN_POINT('',(-1.64992424049175,-3.2,5.51507575950825));
#12855=CARTESIAN_POINT('',(-1.64992424049175,-4.9,5.51507575950825));
#12856=CARTESIAN_POINT('Origin',(-1.48492424049175,-3.2,5.51507575950825));
#12857=CARTESIAN_POINT('Origin',(-1.48492424049175,-4.9,8.48492424049175));
#12858=CARTESIAN_POINT('',(-1.64992424049175,-4.8,8.48492424049175));
#12859=CARTESIAN_POINT('Origin',(-1.48492424049175,-4.8,8.48492424049175));
#12860=CARTESIAN_POINT('',(-1.64992424049175,-3.2,8.48492424049175));
#12861=CARTESIAN_POINT('',(-1.64992424049175,-4.9,8.48492424049175));
#12862=CARTESIAN_POINT('Origin',(-1.48492424049175,-3.2,8.48492424049175));
#12863=CARTESIAN_POINT('Origin',(1.48492424049175,-4.9,8.48492424049175));
#12864=CARTESIAN_POINT('',(1.31992424049175,-4.8,8.48492424049175));
#12865=CARTESIAN_POINT('Origin',(1.48492424049175,-4.8,8.48492424049175));
#12866=CARTESIAN_POINT('',(1.31992424049175,-3.2,8.48492424049175));
#12867=CARTESIAN_POINT('',(1.31992424049175,-4.9,8.48492424049175));
#12868=CARTESIAN_POINT('Origin',(1.48492424049175,-3.2,8.48492424049175));
#12869=CARTESIAN_POINT('Origin',(1.48492424049175,-4.9,5.51507575950825));
#12870=CARTESIAN_POINT('',(1.31992424049175,-4.8,5.51507575950825));
#12871=CARTESIAN_POINT('Origin',(1.48492424049175,-4.8,5.51507575950825));
#12872=CARTESIAN_POINT('',(1.31992424049175,-3.2,5.51507575950825));
#12873=CARTESIAN_POINT('',(1.31992424049175,-4.9,5.51507575950825));
#12874=CARTESIAN_POINT('Origin',(1.48492424049175,-3.2,5.51507575950825));
#12875=CARTESIAN_POINT('Origin',(0.,-4.9,7.));
#12876=CARTESIAN_POINT('',(-1.6,-4.8,7.));
#12877=CARTESIAN_POINT('Origin',(0.,-4.8,7.));
#12878=CARTESIAN_POINT('',(-1.6,-3.2,7.));
#12879=CARTESIAN_POINT('',(-1.6,-4.9,7.));
#12880=CARTESIAN_POINT('Origin',(0.,-3.2,7.));
#12881=CARTESIAN_POINT('Origin',(-2.9,-4.,0.9));
#12882=CARTESIAN_POINT('',(-3.125,-4.,1.));
#12883=CARTESIAN_POINT('Origin',(-2.9,-4.,1.));
#12884=CARTESIAN_POINT('',(-3.125,-4.,1.8));
#12885=CARTESIAN_POINT('',(-3.125,-4.,0.9));
#12886=CARTESIAN_POINT('Origin',(-2.9,-4.,1.8));
#12887=CARTESIAN_POINT('Origin',(2.9,-4.,0.9));
#12888=CARTESIAN_POINT('',(2.675,-4.,1.));
#12889=CARTESIAN_POINT('Origin',(2.9,-4.,1.));
#12890=CARTESIAN_POINT('',(2.675,-4.,1.8));
#12891=CARTESIAN_POINT('',(2.675,-4.,0.9));
#12892=CARTESIAN_POINT('Origin',(2.9,-4.,1.8));
#12893=CARTESIAN_POINT('Origin',(-3.5,-4.8,1.8));
#12894=CARTESIAN_POINT('',(2.4,-4.8,1.8));
#12895=CARTESIAN_POINT('',(2.4,-3.2,1.8));
#12896=CARTESIAN_POINT('',(2.4,-4.8,1.8));
#12897=CARTESIAN_POINT('',(3.5,-4.8,1.8));
#12898=CARTESIAN_POINT('',(3.5,-4.8,1.8));
#12899=CARTESIAN_POINT('',(3.5,-3.2,1.8));
#12900=CARTESIAN_POINT('',(3.5,-4.8,1.8));
#12901=CARTESIAN_POINT('',(3.5,-3.2,1.8));
#12902=CARTESIAN_POINT('Origin',(-3.5,-4.8,1.8));
#12903=CARTESIAN_POINT('',(-2.4,-3.2,1.8));
#12904=CARTESIAN_POINT('',(-2.4,-4.8,1.8));
#12905=CARTESIAN_POINT('',(-2.4,-4.,1.8));
#12906=CARTESIAN_POINT('',(-3.5,-3.2,1.8));
#12907=CARTESIAN_POINT('',(3.5,-3.2,1.8));
#12908=CARTESIAN_POINT('',(-3.5,-4.8,1.8));
#12909=CARTESIAN_POINT('',(-3.5,-4.8,1.8));
#12910=CARTESIAN_POINT('',(3.5,-4.8,1.8));
#12911=CARTESIAN_POINT('Origin',(-3.5,-4.8,1.));
#12912=CARTESIAN_POINT('',(-3.5,-4.8,1.));
#12913=CARTESIAN_POINT('',(-3.5,-4.8,1.8));
#12914=CARTESIAN_POINT('',(-3.5,-3.2,1.));
#12915=CARTESIAN_POINT('',(-3.5,-3.2,1.8));
#12916=CARTESIAN_POINT('',(-3.5,-4.8,1.));
#12917=CARTESIAN_POINT('Origin',(3.5,-4.8,1.8));
#12918=CARTESIAN_POINT('',(3.5,-4.8,1.));
#12919=CARTESIAN_POINT('',(3.5,-4.8,1.));
#12920=CARTESIAN_POINT('',(3.5,-3.2,1.));
#12921=CARTESIAN_POINT('',(3.5,-4.8,1.));
#12922=CARTESIAN_POINT('',(3.5,-3.2,1.));
#12923=CARTESIAN_POINT('Origin',(-2.4,-4.8,1.));
#12924=CARTESIAN_POINT('',(2.4,-4.8,10.));
#12925=CARTESIAN_POINT('',(2.4,-4.8,1.));
#12926=CARTESIAN_POINT('',(-2.4,-4.8,10.));
#12927=CARTESIAN_POINT('',(-2.4,-4.8,10.));
#12928=CARTESIAN_POINT('',(-2.4,-4.8,1.));
#12929=CARTESIAN_POINT('',(-3.5,-4.8,1.));
#12930=CARTESIAN_POINT('Origin',(2.4,-4.8,1.));
#12931=CARTESIAN_POINT('',(2.4,-3.2,10.));
#12932=CARTESIAN_POINT('',(2.4,-3.2,1.));
#12933=CARTESIAN_POINT('',(2.4,-4.8,10.));
#12934=CARTESIAN_POINT('Origin',(2.4,-3.2,1.));
#12935=CARTESIAN_POINT('',(-2.4,-3.2,10.));
#12936=CARTESIAN_POINT('',(-2.4,-3.2,1.));
#12937=CARTESIAN_POINT('',(2.4,-3.2,10.));
#12938=CARTESIAN_POINT('',(-3.5,-3.2,1.));
#12939=CARTESIAN_POINT('Origin',(-2.4,-3.2,1.));
#12940=CARTESIAN_POINT('',(-2.4,-3.2,10.));
#12941=CARTESIAN_POINT('Origin',(0.,-4.,10.));
#12942=CARTESIAN_POINT('Origin',(0.,-4.,1.));
#16950=UNCERTAINTY_MEASURE_WITH_UNIT(LENGTH_MEASURE(0.001),#17047,
'DISTANCE_ACCURACY_VALUE',
'Maximum model space distance between geometric entities at asserted c
onnectivities');
#16993=UNCERTAINTY_MEASURE_WITH_UNIT(LENGTH_MEASURE(0.001),#17047,
'DISTANCE_ACCURACY_VALUE',
'Maximum model space distance between geometric entities at asserted c
onnectivities');
#17003=(
GEOMETRIC_REPRESENTATION_CONTEXT(3)
GLOBAL_UNCERTAINTY_ASSIGNED_CONTEXT((#16950))
GLOBAL_UNIT_ASSIGNED_CONTEXT((#17047,#17049,#17050))
REPRESENTATION_CONTEXT('','3D')
);
#17046=(
GEOMETRIC_REPRESENTATION_CONTEXT(3)
GLOBAL_UNCERTAINTY_ASSIGNED_CONTEXT((#16993))
GLOBAL_UNIT_ASSIGNED_CONTEXT((#17047,#17049,#17050))
REPRESENTATION_CONTEXT('','3D')
);
#17047=(
LENGTH_UNIT()
NAMED_UNIT(*)
SI_UNIT(.CENTI.,.METRE.)
);
#17049=(
NAMED_UNIT(*)
PLANE_ANGLE_UNIT()
SI_UNIT($,.RADIAN.)
);
#17050=(
NAMED_UNIT(*)
SI_UNIT($,.STERADIAN.)
SOLID_ANGLE_UNIT()
);
#17060=SHAPE_DEFINITION_REPRESENTATION(#17112,#17267);
#17112=PRODUCT_DEFINITION_SHAPE('',$,#17320);
#17267=SHAPE_REPRESENTATION('',(#8928),#17003);
#17310=PRODUCT_DEFINITION_CONTEXT('part definition',#17468,'design');
#17320=PRODUCT_DEFINITION('Input bearing carrier (1)',
'Input bearing carrier (1)',#17372,#17310);
#17372=PRODUCT_DEFINITION_FORMATION('',$,#17479);
#17468=APPLICATION_CONTEXT(
'Core Data for Automotive Mechanical Design Process');
#17469=PRODUCT_CONTEXT('part definition',#17468,'mechanical');
#17479=PRODUCT('Input bearing carrier (1)','Input bearing carrier (1)',
'Input bearing carrier (1)',(#17469));
#17585=COLOUR_RGB('Grey',0.48,0.52,0.57);
#17586=FILL_AREA_STYLE_COLOUR('',#17585);
#17587=FILL_AREA_STYLE('',(#17586));
#17588=SURFACE_STYLE_FILL_AREA(#17587);
#17589=SURFACE_SIDE_STYLE('',(#17588));
#17590=SURFACE_STYLE_USAGE(.BOTH.,#17589);
#17591=PRESENTATION_STYLE_ASSIGNMENT((#17590));
ENDSEC;
END-ISO-10303-21;
